ISO-10303-21;
HEADER;
/* Generated by software containing ST-Developer
 * from STEP Tools, Inc. (www.steptools.com) 
 */

FILE_DESCRIPTION(
/* description */ ('Located fixture plate with toggle clamp'),
/* implementation_level */ '2;1');

FILE_NAME(
/* name */ 'Bolt-clearance mounting stand.step',
/* time_stamp */ '2026-10-27T21:36:12-07:00',
/* author */ (''),
/* organization */ (''),
/* preprocessor_version */ 'ST-DEVELOPER v20.2',
/* originating_system */ 'Autodesk Translation Framework v15.17.0.0',
/* authorisation */ '');

FILE_SCHEMA (('AUTOMOTIVE_DESIGN { 1 0 10303 214 3 1 1 }'));
ENDSEC;

DATA;
#10=MECHANICAL_DESIGN_GEOMETRIC_PRESENTATION_REPRESENTATION('',(#322),#9285);
#274=SHAPE_REPRESENTATION_RELATIONSHIP('SRR','None',#9397,#298);
#298=ADVANCED_BREP_SHAPE_REPRESENTATION('',(#346),#9259);
#322=STYLED_ITEM('',(#9619),#346);
#346=MANIFOLD_SOLID_BREP('Body1',#5170);
#379=FACE_BOUND('',#1017,.T.);
#380=FACE_BOUND('',#1018,.T.);
#381=FACE_BOUND('',#1027,.T.);
#382=FACE_BOUND('',#1034,.T.);
#383=FACE_BOUND('',#1038,.T.);
#384=FACE_BOUND('',#1039,.T.);
#513=PLANE('',#5515);
#514=PLANE('',#5516);
#515=PLANE('',#5523);
#516=PLANE('',#5527);
#517=PLANE('',#5528);
#518=PLANE('',#5529);
#519=PLANE('',#5530);
#520=PLANE('',#5531);
#521=PLANE('',#5535);
#522=PLANE('',#5536);
#523=PLANE('',#5537);
#524=PLANE('',#5538);
#525=PLANE('',#5539);
#526=PLANE('',#5540);
#527=PLANE('',#5541);
#528=PLANE('',#5542);
#529=PLANE('',#5543);
#530=PLANE('',#5544);
#531=PLANE('',#5545);
#706=FACE_OUTER_BOUND('',#1014,.T.);
#707=FACE_OUTER_BOUND('',#1015,.T.);
#708=FACE_OUTER_BOUND('',#1016,.T.);
#709=FACE_OUTER_BOUND('',#1019,.T.);
#710=FACE_OUTER_BOUND('',#1020,.T.);
#711=FACE_OUTER_BOUND('',#1021,.T.);
#712=FACE_OUTER_BOUND('',#1022,.T.);
#713=FACE_OUTER_BOUND('',#1023,.T.);
#714=FACE_OUTER_BOUND('',#1024,.T.);
#715=FACE_OUTER_BOUND('',#1025,.T.);
#716=FACE_OUTER_BOUND('',#1026,.T.);
#717=FACE_OUTER_BOUND('',#1028,.T.);
#718=FACE_OUTER_BOUND('',#1029,.T.);
#719=FACE_OUTER_BOUND('',#1030,.T.);
#720=FACE_OUTER_BOUND('',#1031,.T.);
#721=FACE_OUTER_BOUND('',#1032,.T.);
#722=FACE_OUTER_BOUND('',#1033,.T.);
#723=FACE_OUTER_BOUND('',#1035,.T.);
#724=FACE_OUTER_BOUND('',#1036,.T.);
#725=FACE_OUTER_BOUND('',#1037,.T.);
#726=FACE_OUTER_BOUND('',#1040,.T.);
#727=FACE_OUTER_BOUND('',#1041,.T.);
#728=FACE_OUTER_BOUND('',#1042,.T.);
#729=FACE_OUTER_BOUND('',#1043,.T.);
#1014=EDGE_LOOP('',(#3652,#3653,#3654,#3655));
#1015=EDGE_LOOP('',(#3656,#3657));
#1016=EDGE_LOOP('',(#3658,#3659,#3660,#3661,#3662,#3663));
#1017=EDGE_LOOP('',(#3664));
#1018=EDGE_LOOP('',(#3665));
#1019=EDGE_LOOP('',(#3666,#3667,#3668,#3669));
#1020=EDGE_LOOP('',(#3670,#3671,#3672,#3673));
#1021=EDGE_LOOP('',(#3674,#3675,#3676,#3677,#3678,#3679,#3680,#3681));
#1022=EDGE_LOOP('',(#3682,#3683,#3684,#3685));
#1023=EDGE_LOOP('',(#3686));
#1024=EDGE_LOOP('',(#3687,#3688,#3689,#3690));
#1025=EDGE_LOOP('',(#3691,#3692,#3693,#3694));
#1026=EDGE_LOOP('',(#3695,#3696,#3697,#3698));
#1027=EDGE_LOOP('',(#3699));
#1028=EDGE_LOOP('',(#3700,#3701,#3702,#3703));
#1029=EDGE_LOOP('',(#3704,#3705,#3706,#3707));
#1030=EDGE_LOOP('',(#3708));
#1031=EDGE_LOOP('',(#3709,#3710,#3711,#3712));
#1032=EDGE_LOOP('',(#3713,#3714,#3715,#3716));
#1033=EDGE_LOOP('',(#3717,#3718,#3719,#3720));
#1034=EDGE_LOOP('',(#3721));
#1035=EDGE_LOOP('',(#3722,#3723,#3724,#3725));
#1036=EDGE_LOOP('',(#3726,#3727,#3728,#3729));
#1037=EDGE_LOOP('',(#3730,#3731,#3732,#3733));
#1038=EDGE_LOOP('',(#3734));
#1039=EDGE_LOOP('',(#3735));
#1040=EDGE_LOOP('',(#3736,#3737,#3738,#3739,#3740,#3741,#3742,#3743,#3744,
#3745,#3746,#3747,#3748,#3749));
#1041=EDGE_LOOP('',(#3750,#3751,#3752,#3753,#3754,#3755,#3756,#3757,#3758,
#3759,#3760,#3761,#3762,#3763));
#1042=EDGE_LOOP('',(#3764,#3765,#3766,#3767));
#1043=EDGE_LOOP('',(#3768,#3769,#3770,#3771));
#1397=CIRCLE('',#5513,0.6);
#1398=CIRCLE('',#5514,0.6);
#1399=CIRCLE('',#5517,0.33);
#1400=CIRCLE('',#5518,0.33);
#1401=CIRCLE('',#5520,0.33);
#1402=CIRCLE('',#5522,0.33);
#1403=CIRCLE('',#5525,0.210000000000001);
#1404=CIRCLE('',#5526,0.210000000000001);
#1405=CIRCLE('',#5533,0.21);
#1406=CIRCLE('',#5534,0.21);
#1651=LINE('',#7755,#2061);
#1652=LINE('',#7759,#2062);
#1653=LINE('',#7762,#2063);
#1654=LINE('',#7765,#2064);
#1655=LINE('',#7767,#2065);
#1656=LINE('',#7769,#2066);
#1657=LINE('',#7771,#2067);
#1658=LINE('',#7772,#2068);
#1659=LINE('',#7779,#2069);
#1660=LINE('',#7783,#2070);
#1661=LINE('',#7787,#2071);
#1662=LINE('',#7789,#2072);
#1663=LINE('',#7790,#2073);
#1664=LINE('',#7795,#2074);
#1665=LINE('',#7800,#2075);
#1666=LINE('',#7802,#2076);
#1667=LINE('',#7803,#2077);
#1668=LINE('',#7807,#2078);
#1669=LINE('',#7809,#2079);
#1670=LINE('',#7811,#2080);
#1671=LINE('',#7812,#2081);
#1672=LINE('',#7814,#2082);
#1673=LINE('',#7815,#2083);
#1674=LINE('',#7818,#2084);
#1675=LINE('',#7820,#2085);
#1676=LINE('',#7821,#2086);
#1677=LINE('',#7826,#2087);
#1678=LINE('',#7831,#2088);
#1679=LINE('',#7833,#2089);
#1680=LINE('',#7834,#2090);
#1681=LINE('',#7838,#2091);
#1682=LINE('',#7840,#2092);
#1683=LINE('',#7842,#2093);
#1684=LINE('',#7843,#2094);
#1685=LINE('',#7845,#2095);
#1686=LINE('',#7846,#2096);
#1687=LINE('',#7849,#2097);
#1688=LINE('',#7851,#2098);
#1689=LINE('',#7852,#2099);
#1690=LINE('',#7855,#2100);
#1691=LINE('',#7857,#2101);
#1692=LINE('',#7858,#2102);
#1693=LINE('',#7861,#2103);
#1694=LINE('',#7863,#2104);
#1695=LINE('',#7864,#2105);
#1696=LINE('',#7867,#2106);
#1697=LINE('',#7868,#2107);
#1698=LINE('',#7871,#2108);
#1699=LINE('',#7872,#2109);
#1700=LINE('',#7874,#2110);
#2061=VECTOR('',#6203,1.);
#2062=VECTOR('',#6206,1.);
#2063=VECTOR('',#6211,1.);
#2064=VECTOR('',#6214,1.);
#2065=VECTOR('',#6215,1.);
#2066=VECTOR('',#6216,1.);
#2067=VECTOR('',#6217,1.);
#2068=VECTOR('',#6218,1.);
#2069=VECTOR('',#6225,0.33);
#2070=VECTOR('',#6230,0.33);
#2071=VECTOR('',#6235,1.);
#2072=VECTOR('',#6236,1.);
#2073=VECTOR('',#6237,1.);
#2074=VECTOR('',#6242,0.210000000000001);
#2075=VECTOR('',#6249,1.);
#2076=VECTOR('',#6250,1.);
#2077=VECTOR('',#6251,1.);
#2078=VECTOR('',#6254,1.);
#2079=VECTOR('',#6255,1.);
#2080=VECTOR('',#6256,1.);
#2081=VECTOR('',#6257,1.);
#2082=VECTOR('',#6260,1.);
#2083=VECTOR('',#6261,1.);
#2084=VECTOR('',#6264,1.);
#2085=VECTOR('',#6265,1.);
#2086=VECTOR('',#6266,1.);
#2087=VECTOR('',#6271,0.21);
#2088=VECTOR('',#6278,1.);
#2089=VECTOR('',#6279,1.);
#2090=VECTOR('',#6280,1.);
#2091=VECTOR('',#6283,1.);
#2092=VECTOR('',#6284,1.);
#2093=VECTOR('',#6285,1.);
#2094=VECTOR('',#6286,1.);
#2095=VECTOR('',#6289,1.);
#2096=VECTOR('',#6290,1.);
#2097=VECTOR('',#6293,1.);
#2098=VECTOR('',#6294,1.);
#2099=VECTOR('',#6295,1.);
#2100=VECTOR('',#6298,1.);
#2101=VECTOR('',#6299,1.);
#2102=VECTOR('',#6300,1.);
#2103=VECTOR('',#6303,1.);
#2104=VECTOR('',#6304,1.);
#2105=VECTOR('',#6305,1.);
#2106=VECTOR('',#6308,1.);
#2107=VECTOR('',#6309,1.);
#2108=VECTOR('',#6312,1.);
#2109=VECTOR('',#6313,1.);
#2110=VECTOR('',#6316,1.);
#2457=VERTEX_POINT('',#7753);
#2458=VERTEX_POINT('',#7754);
#2459=VERTEX_POINT('',#7756);
#2460=VERTEX_POINT('',#7758);
#2461=VERTEX_POINT('',#7764);
#2462=VERTEX_POINT('',#7766);
#2463=VERTEX_POINT('',#7768);
#2464=VERTEX_POINT('',#7770);
#2465=VERTEX_POINT('',#7773);
#2466=VERTEX_POINT('',#7775);
#2467=VERTEX_POINT('',#7778);
#2468=VERTEX_POINT('',#7782);
#2469=VERTEX_POINT('',#7786);
#2470=VERTEX_POINT('',#7788);
#2471=VERTEX_POINT('',#7792);
#2472=VERTEX_POINT('',#7794);
#2473=VERTEX_POINT('',#7799);
#2474=VERTEX_POINT('',#7801);
#2475=VERTEX_POINT('',#7805);
#2476=VERTEX_POINT('',#7806);
#2477=VERTEX_POINT('',#7808);
#2478=VERTEX_POINT('',#7810);
#2479=VERTEX_POINT('',#7817);
#2480=VERTEX_POINT('',#7819);
#2481=VERTEX_POINT('',#7823);
#2482=VERTEX_POINT('',#7825);
#2483=VERTEX_POINT('',#7830);
#2484=VERTEX_POINT('',#7832);
#2485=VERTEX_POINT('',#7836);
#2486=VERTEX_POINT('',#7837);
#2487=VERTEX_POINT('',#7839);
#2488=VERTEX_POINT('',#7841);
#2489=VERTEX_POINT('',#7848);
#2490=VERTEX_POINT('',#7850);
#2491=VERTEX_POINT('',#7854);
#2492=VERTEX_POINT('',#7856);
#2493=VERTEX_POINT('',#7860);
#2494=VERTEX_POINT('',#7862);
#2495=VERTEX_POINT('',#7866);
#2496=VERTEX_POINT('',#7870);
#2914=EDGE_CURVE('',#2457,#2458,#1651,.T.);
#2915=EDGE_CURVE('',#2459,#2457,#1397,.T.);
#2916=EDGE_CURVE('',#2460,#2459,#1652,.T.);
#2917=EDGE_CURVE('',#2460,#2458,#1398,.T.);
#2918=EDGE_CURVE('',#2459,#2457,#1653,.T.);
#2919=EDGE_CURVE('',#2461,#2460,#1654,.T.);
#2920=EDGE_CURVE('',#2462,#2461,#1655,.T.);
#2921=EDGE_CURVE('',#2463,#2462,#1656,.T.);
#2922=EDGE_CURVE('',#2464,#2463,#1657,.T.);
#2923=EDGE_CURVE('',#2458,#2464,#1658,.T.);
#2924=EDGE_CURVE('',#2465,#2465,#1399,.T.);
#2925=EDGE_CURVE('',#2466,#2466,#1400,.T.);
#2926=EDGE_CURVE('',#2466,#2467,#1659,.T.);
#2927=EDGE_CURVE('',#2467,#2467,#1401,.T.);
#2928=EDGE_CURVE('',#2465,#2468,#1660,.T.);
#2929=EDGE_CURVE('',#2468,#2468,#1402,.T.);
#2930=EDGE_CURVE('',#2464,#2469,#1661,.T.);
#2931=EDGE_CURVE('',#2469,#2470,#1662,.T.);
#2932=EDGE_CURVE('',#2470,#2461,#1663,.T.);
#2933=EDGE_CURVE('',#2471,#2471,#1403,.T.);
#2934=EDGE_CURVE('',#2471,#2472,#1664,.T.);
#2935=EDGE_CURVE('',#2472,#2472,#1404,.T.);
#2936=EDGE_CURVE('',#2469,#2473,#1665,.T.);
#2937=EDGE_CURVE('',#2474,#2473,#1666,.T.);
#2938=EDGE_CURVE('',#2470,#2474,#1667,.T.);
#2939=EDGE_CURVE('',#2475,#2476,#1668,.T.);
#2940=EDGE_CURVE('',#2475,#2477,#1669,.T.);
#2941=EDGE_CURVE('',#2478,#2477,#1670,.T.);
#2942=EDGE_CURVE('',#2476,#2478,#1671,.T.);
#2943=EDGE_CURVE('',#2477,#2474,#1672,.T.);
#2944=EDGE_CURVE('',#2473,#2478,#1673,.T.);
#2945=EDGE_CURVE('',#2476,#2479,#1674,.T.);
#2946=EDGE_CURVE('',#2479,#2480,#1675,.T.);
#2947=EDGE_CURVE('',#2480,#2475,#1676,.T.);
#2948=EDGE_CURVE('',#2481,#2481,#1405,.T.);
#2949=EDGE_CURVE('',#2481,#2482,#1677,.T.);
#2950=EDGE_CURVE('',#2482,#2482,#1406,.T.);
#2951=EDGE_CURVE('',#2479,#2483,#1678,.T.);
#2952=EDGE_CURVE('',#2484,#2483,#1679,.T.);
#2953=EDGE_CURVE('',#2480,#2484,#1680,.T.);
#2954=EDGE_CURVE('',#2485,#2486,#1681,.T.);
#2955=EDGE_CURVE('',#2485,#2487,#1682,.T.);
#2956=EDGE_CURVE('',#2488,#2487,#1683,.T.);
#2957=EDGE_CURVE('',#2486,#2488,#1684,.T.);
#2958=EDGE_CURVE('',#2487,#2484,#1685,.T.);
#2959=EDGE_CURVE('',#2483,#2488,#1686,.T.);
#2960=EDGE_CURVE('',#2486,#2489,#1687,.T.);
#2961=EDGE_CURVE('',#2489,#2490,#1688,.T.);
#2962=EDGE_CURVE('',#2490,#2485,#1689,.T.);
#2963=EDGE_CURVE('',#2462,#2491,#1690,.T.);
#2964=EDGE_CURVE('',#2492,#2491,#1691,.T.);
#2965=EDGE_CURVE('',#2463,#2492,#1692,.T.);
#2966=EDGE_CURVE('',#2491,#2493,#1693,.T.);
#2967=EDGE_CURVE('',#2493,#2494,#1694,.T.);
#2968=EDGE_CURVE('',#2494,#2492,#1695,.T.);
#2969=EDGE_CURVE('',#2495,#2494,#1696,.T.);
#2970=EDGE_CURVE('',#2495,#2489,#1697,.T.);
#2971=EDGE_CURVE('',#2496,#2493,#1698,.T.);
#2972=EDGE_CURVE('',#2496,#2490,#1699,.T.);
#2973=EDGE_CURVE('',#2495,#2496,#1700,.T.);
#3652=ORIENTED_EDGE('',*,*,#2914,.F.);
#3653=ORIENTED_EDGE('',*,*,#2915,.F.);
#3654=ORIENTED_EDGE('',*,*,#2916,.F.);
#3655=ORIENTED_EDGE('',*,*,#2917,.T.);
#3656=ORIENTED_EDGE('',*,*,#2918,.F.);
#3657=ORIENTED_EDGE('',*,*,#2915,.T.);
#3658=ORIENTED_EDGE('',*,*,#2919,.F.);
#3659=ORIENTED_EDGE('',*,*,#2920,.F.);
#3660=ORIENTED_EDGE('',*,*,#2921,.F.);
#3661=ORIENTED_EDGE('',*,*,#2922,.F.);
#3662=ORIENTED_EDGE('',*,*,#2923,.F.);
#3663=ORIENTED_EDGE('',*,*,#2917,.F.);
#3664=ORIENTED_EDGE('',*,*,#2924,.T.);
#3665=ORIENTED_EDGE('',*,*,#2925,.T.);
#3666=ORIENTED_EDGE('',*,*,#2925,.F.);
#3667=ORIENTED_EDGE('',*,*,#2926,.T.);
#3668=ORIENTED_EDGE('',*,*,#2927,.F.);
#3669=ORIENTED_EDGE('',*,*,#2926,.F.);
#3670=ORIENTED_EDGE('',*,*,#2924,.F.);
#3671=ORIENTED_EDGE('',*,*,#2928,.T.);
#3672=ORIENTED_EDGE('',*,*,#2929,.F.);
#3673=ORIENTED_EDGE('',*,*,#2928,.F.);
#3674=ORIENTED_EDGE('',*,*,#2914,.T.);
#3675=ORIENTED_EDGE('',*,*,#2923,.T.);
#3676=ORIENTED_EDGE('',*,*,#2930,.T.);
#3677=ORIENTED_EDGE('',*,*,#2931,.T.);
#3678=ORIENTED_EDGE('',*,*,#2932,.T.);
#3679=ORIENTED_EDGE('',*,*,#2919,.T.);
#3680=ORIENTED_EDGE('',*,*,#2916,.T.);
#3681=ORIENTED_EDGE('',*,*,#2918,.T.);
#3682=ORIENTED_EDGE('',*,*,#2933,.F.);
#3683=ORIENTED_EDGE('',*,*,#2934,.T.);
#3684=ORIENTED_EDGE('',*,*,#2935,.F.);
#3685=ORIENTED_EDGE('',*,*,#2934,.F.);
#3686=ORIENTED_EDGE('',*,*,#2933,.T.);
#3687=ORIENTED_EDGE('',*,*,#2931,.F.);
#3688=ORIENTED_EDGE('',*,*,#2936,.T.);
#3689=ORIENTED_EDGE('',*,*,#2937,.F.);
#3690=ORIENTED_EDGE('',*,*,#2938,.F.);
#3691=ORIENTED_EDGE('',*,*,#2939,.F.);
#3692=ORIENTED_EDGE('',*,*,#2940,.T.);
#3693=ORIENTED_EDGE('',*,*,#2941,.F.);
#3694=ORIENTED_EDGE('',*,*,#2942,.F.);
#3695=ORIENTED_EDGE('',*,*,#2941,.T.);
#3696=ORIENTED_EDGE('',*,*,#2943,.T.);
#3697=ORIENTED_EDGE('',*,*,#2937,.T.);
#3698=ORIENTED_EDGE('',*,*,#2944,.T.);
#3699=ORIENTED_EDGE('',*,*,#2935,.T.);
#3700=ORIENTED_EDGE('',*,*,#2939,.T.);
#3701=ORIENTED_EDGE('',*,*,#2945,.T.);
#3702=ORIENTED_EDGE('',*,*,#2946,.T.);
#3703=ORIENTED_EDGE('',*,*,#2947,.T.);
#3704=ORIENTED_EDGE('',*,*,#2948,.F.);
#3705=ORIENTED_EDGE('',*,*,#2949,.T.);
#3706=ORIENTED_EDGE('',*,*,#2950,.F.);
#3707=ORIENTED_EDGE('',*,*,#2949,.F.);
#3708=ORIENTED_EDGE('',*,*,#2948,.T.);
#3709=ORIENTED_EDGE('',*,*,#2946,.F.);
#3710=ORIENTED_EDGE('',*,*,#2951,.T.);
#3711=ORIENTED_EDGE('',*,*,#2952,.F.);
#3712=ORIENTED_EDGE('',*,*,#2953,.F.);
#3713=ORIENTED_EDGE('',*,*,#2954,.F.);
#3714=ORIENTED_EDGE('',*,*,#2955,.T.);
#3715=ORIENTED_EDGE('',*,*,#2956,.F.);
#3716=ORIENTED_EDGE('',*,*,#2957,.F.);
#3717=ORIENTED_EDGE('',*,*,#2956,.T.);
#3718=ORIENTED_EDGE('',*,*,#2958,.T.);
#3719=ORIENTED_EDGE('',*,*,#2952,.T.);
#3720=ORIENTED_EDGE('',*,*,#2959,.T.);
#3721=ORIENTED_EDGE('',*,*,#2950,.T.);
#3722=ORIENTED_EDGE('',*,*,#2954,.T.);
#3723=ORIENTED_EDGE('',*,*,#2960,.T.);
#3724=ORIENTED_EDGE('',*,*,#2961,.T.);
#3725=ORIENTED_EDGE('',*,*,#2962,.T.);
#3726=ORIENTED_EDGE('',*,*,#2921,.T.);
#3727=ORIENTED_EDGE('',*,*,#2963,.T.);
#3728=ORIENTED_EDGE('',*,*,#2964,.F.);
#3729=ORIENTED_EDGE('',*,*,#2965,.F.);
#3730=ORIENTED_EDGE('',*,*,#2966,.T.);
#3731=ORIENTED_EDGE('',*,*,#2967,.T.);
#3732=ORIENTED_EDGE('',*,*,#2968,.T.);
#3733=ORIENTED_EDGE('',*,*,#2964,.T.);
#3734=ORIENTED_EDGE('',*,*,#2927,.T.);
#3735=ORIENTED_EDGE('',*,*,#2929,.T.);
#3736=ORIENTED_EDGE('',*,*,#2969,.F.);
#3737=ORIENTED_EDGE('',*,*,#2970,.T.);
#3738=ORIENTED_EDGE('',*,*,#2960,.F.);
#3739=ORIENTED_EDGE('',*,*,#2957,.T.);
#3740=ORIENTED_EDGE('',*,*,#2959,.F.);
#3741=ORIENTED_EDGE('',*,*,#2951,.F.);
#3742=ORIENTED_EDGE('',*,*,#2945,.F.);
#3743=ORIENTED_EDGE('',*,*,#2942,.T.);
#3744=ORIENTED_EDGE('',*,*,#2944,.F.);
#3745=ORIENTED_EDGE('',*,*,#2936,.F.);
#3746=ORIENTED_EDGE('',*,*,#2930,.F.);
#3747=ORIENTED_EDGE('',*,*,#2922,.T.);
#3748=ORIENTED_EDGE('',*,*,#2965,.T.);
#3749=ORIENTED_EDGE('',*,*,#2968,.F.);
#3750=ORIENTED_EDGE('',*,*,#2971,.T.);
#3751=ORIENTED_EDGE('',*,*,#2966,.F.);
#3752=ORIENTED_EDGE('',*,*,#2963,.F.);
#3753=ORIENTED_EDGE('',*,*,#2920,.T.);
#3754=ORIENTED_EDGE('',*,*,#2932,.F.);
#3755=ORIENTED_EDGE('',*,*,#2938,.T.);
#3756=ORIENTED_EDGE('',*,*,#2943,.F.);
#3757=ORIENTED_EDGE('',*,*,#2940,.F.);
#3758=ORIENTED_EDGE('',*,*,#2947,.F.);
#3759=ORIENTED_EDGE('',*,*,#2953,.T.);
#3760=ORIENTED_EDGE('',*,*,#2958,.F.);
#3761=ORIENTED_EDGE('',*,*,#2955,.F.);
#3762=ORIENTED_EDGE('',*,*,#2962,.F.);
#3763=ORIENTED_EDGE('',*,*,#2972,.F.);
#3764=ORIENTED_EDGE('',*,*,#2973,.T.);
#3765=ORIENTED_EDGE('',*,*,#2972,.T.);
#3766=ORIENTED_EDGE('',*,*,#2961,.F.);
#3767=ORIENTED_EDGE('',*,*,#2970,.F.);
#3768=ORIENTED_EDGE('',*,*,#2973,.F.);
#3769=ORIENTED_EDGE('',*,*,#2969,.T.);
#3770=ORIENTED_EDGE('',*,*,#2967,.F.);
#3771=ORIENTED_EDGE('',*,*,#2971,.F.);
#4798=CYLINDRICAL_SURFACE('',#5512,0.6);
#4799=CYLINDRICAL_SURFACE('',#5519,0.33);
#4800=CYLINDRICAL_SURFACE('',#5521,0.33);
#4801=CYLINDRICAL_SURFACE('',#5524,0.210000000000001);
#4802=CYLINDRICAL_SURFACE('',#5532,0.21);
#4907=ADVANCED_FACE('',(#706),#4798,.F.);
#4908=ADVANCED_FACE('',(#707),#513,.T.);
#4909=ADVANCED_FACE('',(#708,#379,#380),#514,.F.);
#4910=ADVANCED_FACE('',(#709),#4799,.F.);
#4911=ADVANCED_FACE('',(#710),#4800,.F.);
#4912=ADVANCED_FACE('',(#711),#515,.T.);
#4913=ADVANCED_FACE('',(#712),#4801,.F.);
#4914=ADVANCED_FACE('',(#713),#516,.T.);
#4915=ADVANCED_FACE('',(#714),#517,.T.);
#4916=ADVANCED_FACE('',(#715),#518,.T.);
#4917=ADVANCED_FACE('',(#716,#381),#519,.T.);
#4918=ADVANCED_FACE('',(#717),#520,.T.);
#4919=ADVANCED_FACE('',(#718),#4802,.F.);
#4920=ADVANCED_FACE('',(#719),#521,.T.);
#4921=ADVANCED_FACE('',(#720),#522,.T.);
#4922=ADVANCED_FACE('',(#721),#523,.T.);
#4923=ADVANCED_FACE('',(#722,#382),#524,.T.);
#4924=ADVANCED_FACE('',(#723),#525,.T.);
#4925=ADVANCED_FACE('',(#724),#526,.T.);
#4926=ADVANCED_FACE('',(#725,#383,#384),#527,.T.);
#4927=ADVANCED_FACE('',(#726),#528,.T.);
#4928=ADVANCED_FACE('',(#727),#529,.T.);
#4929=ADVANCED_FACE('',(#728),#530,.T.);
#4930=ADVANCED_FACE('',(#729),#531,.F.);
#5170=CLOSED_SHELL('',(#4907,#4908,#4909,#4910,#4911,#4912,#4913,#4914,
#4915,#4916,#4917,#4918,#4919,#4920,#4921,#4922,#4923,#4924,#4925,#4926,
#4927,#4928,#4929,#4930));
#5511=AXIS2_PLACEMENT_3D('',#7751,#6199,#6200);
#5512=AXIS2_PLACEMENT_3D('',#7752,#6201,#6202);
#5513=AXIS2_PLACEMENT_3D('',#7757,#6204,#6205);
#5514=AXIS2_PLACEMENT_3D('',#7760,#6207,#6208);
#5515=AXIS2_PLACEMENT_3D('',#7761,#6209,#6210);
#5516=AXIS2_PLACEMENT_3D('',#7763,#6212,#6213);
#5517=AXIS2_PLACEMENT_3D('',#7774,#6219,#6220);
#5518=AXIS2_PLACEMENT_3D('',#7776,#6221,#6222);
#5519=AXIS2_PLACEMENT_3D('',#7777,#6223,#6224);
#5520=AXIS2_PLACEMENT_3D('',#7780,#6226,#6227);
#5521=AXIS2_PLACEMENT_3D('',#7781,#6228,#6229);
#5522=AXIS2_PLACEMENT_3D('',#7784,#6231,#6232);
#5523=AXIS2_PLACEMENT_3D('',#7785,#6233,#6234);
#5524=AXIS2_PLACEMENT_3D('',#7791,#6238,#6239);
#5525=AXIS2_PLACEMENT_3D('',#7793,#6240,#6241);
#5526=AXIS2_PLACEMENT_3D('',#7796,#6243,#6244);
#5527=AXIS2_PLACEMENT_3D('',#7797,#6245,#6246);
#5528=AXIS2_PLACEMENT_3D('',#7798,#6247,#6248);
#5529=AXIS2_PLACEMENT_3D('',#7804,#6252,#6253);
#5530=AXIS2_PLACEMENT_3D('',#7813,#6258,#6259);
#5531=AXIS2_PLACEMENT_3D('',#7816,#6262,#6263);
#5532=AXIS2_PLACEMENT_3D('',#7822,#6267,#6268);
#5533=AXIS2_PLACEMENT_3D('',#7824,#6269,#6270);
#5534=AXIS2_PLACEMENT_3D('',#7827,#6272,#6273);
#5535=AXIS2_PLACEMENT_3D('',#7828,#6274,#6275);
#5536=AXIS2_PLACEMENT_3D('',#7829,#6276,#6277);
#5537=AXIS2_PLACEMENT_3D('',#7835,#6281,#6282);
#5538=AXIS2_PLACEMENT_3D('',#7844,#6287,#6288);
#5539=AXIS2_PLACEMENT_3D('',#7847,#6291,#6292);
#5540=AXIS2_PLACEMENT_3D('',#7853,#6296,#6297);
#5541=AXIS2_PLACEMENT_3D('',#7859,#6301,#6302);
#5542=AXIS2_PLACEMENT_3D('',#7865,#6306,#6307);
#5543=AXIS2_PLACEMENT_3D('',#7869,#6310,#6311);
#5544=AXIS2_PLACEMENT_3D('',#7873,#6314,#6315);
#5545=AXIS2_PLACEMENT_3D('',#7875,#6317,#6318);
#6199=DIRECTION('axis',(0.,0.,1.));
#6200=DIRECTION('refdir',(1.,0.,0.));
#6201=DIRECTION('center_axis',(1.,0.,0.));
#6202=DIRECTION('ref_axis',(0.,0.,-1.));
#6203=DIRECTION('',(1.,0.,0.));
#6204=DIRECTION('center_axis',(1.,0.,0.));
#6205=DIRECTION('ref_axis',(0.,0.,-1.));
#6206=DIRECTION('',(-1.,0.,0.));
#6207=DIRECTION('center_axis',(1.,0.,0.));
#6208=DIRECTION('ref_axis',(0.,0.,-1.));
#6209=DIRECTION('center_axis',(1.,0.,0.));
#6210=DIRECTION('ref_axis',(0.,0.,-1.));
#6211=DIRECTION('',(0.,1.,0.));
#6212=DIRECTION('center_axis',(1.,0.,0.));
#6213=DIRECTION('ref_axis',(0.,0.,-1.));
#6214=DIRECTION('',(0.,1.,0.));
#6215=DIRECTION('',(0.,0.,-1.));
#6216=DIRECTION('',(0.,-1.,0.));
#6217=DIRECTION('',(0.,0.,1.));
#6218=DIRECTION('',(0.,1.,0.));
#6219=DIRECTION('center_axis',(1.,0.,0.));
#6220=DIRECTION('ref_axis',(0.,0.,-1.));
#6221=DIRECTION('center_axis',(1.,0.,0.));
#6222=DIRECTION('ref_axis',(0.,0.,-1.));
#6223=DIRECTION('center_axis',(1.,0.,0.));
#6224=DIRECTION('ref_axis',(0.,0.,-1.));
#6225=DIRECTION('',(1.,0.,0.));
#6226=DIRECTION('center_axis',(-1.,0.,0.));
#6227=DIRECTION('ref_axis',(0.,0.,-1.));
#6228=DIRECTION('center_axis',(1.,0.,0.));
#6229=DIRECTION('ref_axis',(0.,0.,-1.));
#6230=DIRECTION('',(1.,0.,0.));
#6231=DIRECTION('center_axis',(-1.,0.,0.));
#6232=DIRECTION('ref_axis',(0.,0.,-1.));
#6233=DIRECTION('center_axis',(0.,0.,1.));
#6234=DIRECTION('ref_axis',(1.,0.,0.));
#6235=DIRECTION('',(-1.,0.,0.));
#6236=DIRECTION('',(0.,-1.,0.));
#6237=DIRECTION('',(1.,0.,0.));
#6238=DIRECTION('center_axis',(0.,0.,1.));
#6239=DIRECTION('ref_axis',(1.,0.,0.));
#6240=DIRECTION('center_axis',(0.,0.,1.));
#6241=DIRECTION('ref_axis',(1.,0.,0.));
#6242=DIRECTION('',(0.,0.,1.));
#6243=DIRECTION('center_axis',(0.,0.,-1.));
#6244=DIRECTION('ref_axis',(1.,0.,0.));
#6245=DIRECTION('center_axis',(0.,0.,1.));
#6246=DIRECTION('ref_axis',(1.,0.,0.));
#6247=DIRECTION('center_axis',(1.,0.,0.));
#6248=DIRECTION('ref_axis',(0.,1.,0.));
#6249=DIRECTION('',(0.,0.,1.));
#6250=DIRECTION('',(0.,1.,0.));
#6251=DIRECTION('',(0.,0.,1.));
#6252=DIRECTION('center_axis',(-1.,0.,0.));
#6253=DIRECTION('ref_axis',(0.,-1.,0.));
#6254=DIRECTION('',(0.,1.,0.));
#6255=DIRECTION('',(0.,0.,1.));
#6256=DIRECTION('',(0.,-1.,0.));
#6257=DIRECTION('',(0.,0.,1.));
#6258=DIRECTION('center_axis',(0.,0.,1.));
#6259=DIRECTION('ref_axis',(1.,0.,0.));
#6260=DIRECTION('',(1.,0.,0.));
#6261=DIRECTION('',(-1.,0.,0.));
#6262=DIRECTION('center_axis',(0.,0.,1.));
#6263=DIRECTION('ref_axis',(1.,0.,0.));
#6264=DIRECTION('',(-1.,0.,0.));
#6265=DIRECTION('',(0.,-1.,0.));
#6266=DIRECTION('',(1.,0.,0.));
#6267=DIRECTION('center_axis',(0.,0.,1.));
#6268=DIRECTION('ref_axis',(1.,0.,0.));
#6269=DIRECTION('center_axis',(0.,0.,1.));
#6270=DIRECTION('ref_axis',(1.,0.,0.));
#6271=DIRECTION('',(0.,0.,1.));
#6272=DIRECTION('center_axis',(0.,0.,-1.));
#6273=DIRECTION('ref_axis',(1.,0.,0.));
#6274=DIRECTION('center_axis',(0.,0.,1.));
#6275=DIRECTION('ref_axis',(1.,0.,0.));
#6276=DIRECTION('center_axis',(1.,0.,0.));
#6277=DIRECTION('ref_axis',(0.,1.,0.));
#6278=DIRECTION('',(0.,0.,1.));
#6279=DIRECTION('',(0.,1.,0.));
#6280=DIRECTION('',(0.,0.,1.));
#6281=DIRECTION('center_axis',(-1.,0.,0.));
#6282=DIRECTION('ref_axis',(0.,-1.,0.));
#6283=DIRECTION('',(0.,1.,0.));
#6284=DIRECTION('',(0.,0.,1.));
#6285=DIRECTION('',(0.,-1.,0.));
#6286=DIRECTION('',(0.,0.,1.));
#6287=DIRECTION('center_axis',(0.,0.,1.));
#6288=DIRECTION('ref_axis',(1.,0.,0.));
#6289=DIRECTION('',(1.,0.,0.));
#6290=DIRECTION('',(-1.,0.,0.));
#6291=DIRECTION('center_axis',(0.,0.,1.));
#6292=DIRECTION('ref_axis',(1.,0.,0.));
#6293=DIRECTION('',(-1.,0.,0.));
#6294=DIRECTION('',(0.,-1.,0.));
#6295=DIRECTION('',(1.,0.,0.));
#6296=DIRECTION('center_axis',(0.,0.,1.));
#6297=DIRECTION('ref_axis',(0.,-1.,0.));
#6298=DIRECTION('',(1.,0.,0.));
#6299=DIRECTION('',(0.,-1.,0.));
#6300=DIRECTION('',(1.,0.,0.));
#6301=DIRECTION('center_axis',(1.,0.,0.));
#6302=DIRECTION('ref_axis',(0.,0.,-1.));
#6303=DIRECTION('',(0.,0.,-1.));
#6304=DIRECTION('',(0.,1.,0.));
#6305=DIRECTION('',(0.,0.,1.));
#6306=DIRECTION('center_axis',(0.,1.,0.));
#6307=DIRECTION('ref_axis',(-1.,0.,0.));
#6308=DIRECTION('',(1.,0.,0.));
#6309=DIRECTION('',(0.,0.,1.));
#6310=DIRECTION('center_axis',(0.,-1.,0.));
#6311=DIRECTION('ref_axis',(1.,0.,0.));
#6312=DIRECTION('',(1.,0.,0.));
#6313=DIRECTION('',(0.,0.,1.));
#6314=DIRECTION('center_axis',(-1.,0.,0.));
#6315=DIRECTION('ref_axis',(0.,-1.,0.));
#6316=DIRECTION('',(0.,-1.,0.));
#6317=DIRECTION('center_axis',(0.,0.,1.));
#6318=DIRECTION('ref_axis',(1.,0.,0.));
#7751=CARTESIAN_POINT('',(0.,0.,0.));
#7752=CARTESIAN_POINT('Origin',(17.3,0.,-0.8));
#7753=CARTESIAN_POINT('',(17.3,0.519615242270663,-0.5));
#7754=CARTESIAN_POINT('',(18.,0.519615242270663,-0.5));
#7755=CARTESIAN_POINT('',(17.3,0.519615242270663,-0.5));
#7756=CARTESIAN_POINT('',(17.3,-0.519615242270663,-0.5));
#7757=CARTESIAN_POINT('Origin',(17.3,0.,-0.8));
#7758=CARTESIAN_POINT('',(18.,-0.519615242270663,-0.5));
#7759=CARTESIAN_POINT('',(17.3,-0.519615242270663,-0.5));
#7760=CARTESIAN_POINT('Origin',(18.,0.,-0.8));
#7761=CARTESIAN_POINT('Origin',(17.3,0.,-0.8));
#7762=CARTESIAN_POINT('',(17.3,0.,-0.5));
#7763=CARTESIAN_POINT('Origin',(18.,0.,1.75));
#7764=CARTESIAN_POINT('',(18.,-1.25,-0.5));
#7765=CARTESIAN_POINT('',(18.,-1.25,-0.5));
#7766=CARTESIAN_POINT('',(18.,-1.25,5.));
#7767=CARTESIAN_POINT('',(18.,-1.25,5.));
#7768=CARTESIAN_POINT('',(18.,1.25,5.));
#7769=CARTESIAN_POINT('',(18.,1.25,5.));
#7770=CARTESIAN_POINT('',(18.,1.25,-0.5));
#7771=CARTESIAN_POINT('',(18.,1.25,-1.5));
#7772=CARTESIAN_POINT('',(18.,-1.25,-0.5));
#7773=CARTESIAN_POINT('',(18.,-4.04133443718627E-17,4.33));
#7774=CARTESIAN_POINT('Origin',(18.,0.,4.));
#7775=CARTESIAN_POINT('',(18.,-4.04133443718626E-17,-0.47));
#7776=CARTESIAN_POINT('Origin',(18.,0.,-0.8));
#7777=CARTESIAN_POINT('Origin',(17.9,0.,-0.8));
#7778=CARTESIAN_POINT('',(18.8,4.04133443718626E-17,-0.47));
#7779=CARTESIAN_POINT('',(17.9,-4.04133443718626E-17,-0.47));
#7780=CARTESIAN_POINT('Origin',(18.8,0.,-0.8));
#7781=CARTESIAN_POINT('Origin',(17.9,0.,4.));
#7782=CARTESIAN_POINT('',(18.8,4.04133443718627E-17,4.33));
#7783=CARTESIAN_POINT('',(17.9,-4.04133443718627E-17,4.33));
#7784=CARTESIAN_POINT('Origin',(18.8,0.,4.));
#7785=CARTESIAN_POINT('Origin',(8.,0.,-0.5));
#7786=CARTESIAN_POINT('',(11.,1.25,-0.5));
#7787=CARTESIAN_POINT('',(18.,1.25,-0.5));
#7788=CARTESIAN_POINT('',(11.,-1.25,-0.5));
#7789=CARTESIAN_POINT('',(11.,-0.625,-0.5));
#7790=CARTESIAN_POINT('',(-2.,-1.25,-0.5));
#7791=CARTESIAN_POINT('Origin',(10.5,0.,-1.2));
#7792=CARTESIAN_POINT('',(10.29,-2.57175827820945E-17,-1.2));
#7793=CARTESIAN_POINT('Origin',(10.5,0.,-1.2));
#7794=CARTESIAN_POINT('',(10.29,2.57175827820945E-17,0.));
#7795=CARTESIAN_POINT('',(10.29,-2.57175827820945E-17,-1.2));
#7796=CARTESIAN_POINT('Origin',(10.5,0.,0.));
#7797=CARTESIAN_POINT('Origin',(10.5,0.,-1.2));
#7798=CARTESIAN_POINT('Origin',(11.,-1.25,-0.5));
#7799=CARTESIAN_POINT('',(11.,1.25,0.));
#7800=CARTESIAN_POINT('',(11.,1.25,-0.5));
#7801=CARTESIAN_POINT('',(11.,-1.25,0.));
#7802=CARTESIAN_POINT('',(11.,-1.25,0.));
#7803=CARTESIAN_POINT('',(11.,-1.25,-0.5));
#7804=CARTESIAN_POINT('Origin',(10.,1.25,-0.5));
#7805=CARTESIAN_POINT('',(10.,-1.25,-0.5));
#7806=CARTESIAN_POINT('',(10.,1.25,-0.5));
#7807=CARTESIAN_POINT('',(10.,0.625,-0.5));
#7808=CARTESIAN_POINT('',(10.,-1.25,0.));
#7809=CARTESIAN_POINT('',(10.,-1.25,-0.5));
#7810=CARTESIAN_POINT('',(10.,1.25,0.));
#7811=CARTESIAN_POINT('',(10.,1.25,0.));
#7812=CARTESIAN_POINT('',(10.,1.25,-0.5));
#7813=CARTESIAN_POINT('Origin',(10.5,0.,0.));
#7814=CARTESIAN_POINT('',(10.,-1.25,0.));
#7815=CARTESIAN_POINT('',(11.,1.25,0.));
#7816=CARTESIAN_POINT('Origin',(8.,0.,-0.5));
#7817=CARTESIAN_POINT('',(-0.7,1.25,-0.5));
#7818=CARTESIAN_POINT('',(18.,1.25,-0.5));
#7819=CARTESIAN_POINT('',(-0.7,-1.25,-0.5));
#7820=CARTESIAN_POINT('',(-0.7,-0.625,-0.5));
#7821=CARTESIAN_POINT('',(-2.,-1.25,-0.5));
#7822=CARTESIAN_POINT('Origin',(-1.2,0.,-1.2));
#7823=CARTESIAN_POINT('',(-1.41,-2.57175827820944E-17,-1.2));
#7824=CARTESIAN_POINT('Origin',(-1.2,0.,-1.2));
#7825=CARTESIAN_POINT('',(-1.41,2.57175827820944E-17,0.));
#7826=CARTESIAN_POINT('',(-1.41,-2.57175827820944E-17,-1.2));
#7827=CARTESIAN_POINT('Origin',(-1.2,0.,0.));
#7828=CARTESIAN_POINT('Origin',(-1.2,0.,-1.2));
#7829=CARTESIAN_POINT('Origin',(-0.7,-1.25,-0.5));
#7830=CARTESIAN_POINT('',(-0.7,1.25,0.));
#7831=CARTESIAN_POINT('',(-0.7,1.25,-0.5));
#7832=CARTESIAN_POINT('',(-0.7,-1.25,0.));
#7833=CARTESIAN_POINT('',(-0.7,-1.25,0.));
#7834=CARTESIAN_POINT('',(-0.7,-1.25,-0.5));
#7835=CARTESIAN_POINT('Origin',(-1.7,1.25,-0.5));
#7836=CARTESIAN_POINT('',(-1.7,-1.25,-0.5));
#7837=CARTESIAN_POINT('',(-1.7,1.25,-0.5));
#7838=CARTESIAN_POINT('',(-1.7,0.625,-0.5));
#7839=CARTESIAN_POINT('',(-1.7,-1.25,0.));
#7840=CARTESIAN_POINT('',(-1.7,-1.25,-0.5));
#7841=CARTESIAN_POINT('',(-1.7,1.25,0.));
#7842=CARTESIAN_POINT('',(-1.7,1.25,0.));
#7843=CARTESIAN_POINT('',(-1.7,1.25,-0.5));
#7844=CARTESIAN_POINT('Origin',(-1.2,0.,0.));
#7845=CARTESIAN_POINT('',(-1.7,-1.25,0.));
#7846=CARTESIAN_POINT('',(-0.7,1.25,0.));
#7847=CARTESIAN_POINT('Origin',(8.,0.,-0.5));
#7848=CARTESIAN_POINT('',(-2.,1.25,-0.5));
#7849=CARTESIAN_POINT('',(18.,1.25,-0.5));
#7850=CARTESIAN_POINT('',(-2.,-1.25,-0.5));
#7851=CARTESIAN_POINT('',(-2.,1.25,-0.5));
#7852=CARTESIAN_POINT('',(-2.,-1.25,-0.5));
#7853=CARTESIAN_POINT('Origin',(18.,1.25,5.));
#7854=CARTESIAN_POINT('',(18.8,-1.25,5.));
#7855=CARTESIAN_POINT('',(18.,-1.25,5.));
#7856=CARTESIAN_POINT('',(18.8,1.25,5.));
#7857=CARTESIAN_POINT('',(18.8,1.25,5.));
#7858=CARTESIAN_POINT('',(18.,1.25,5.));
#7859=CARTESIAN_POINT('Origin',(18.8,0.,1.75));
#7860=CARTESIAN_POINT('',(18.8,-1.25,-1.5));
#7861=CARTESIAN_POINT('',(18.8,-1.25,5.));
#7862=CARTESIAN_POINT('',(18.8,1.25,-1.5));
#7863=CARTESIAN_POINT('',(18.8,-1.25,-1.5));
#7864=CARTESIAN_POINT('',(18.8,1.25,-1.5));
#7865=CARTESIAN_POINT('Origin',(18.,1.25,-1.5));
#7866=CARTESIAN_POINT('',(-2.,1.25,-1.5));
#7867=CARTESIAN_POINT('',(18.,1.25,-1.5));
#7868=CARTESIAN_POINT('',(-2.,1.25,-1.5));
#7869=CARTESIAN_POINT('Origin',(-2.,-1.25,-1.5));
#7870=CARTESIAN_POINT('',(-2.,-1.25,-1.5));
#7871=CARTESIAN_POINT('',(-2.,-1.25,-1.5));
#7872=CARTESIAN_POINT('',(-2.,-1.25,-1.5));
#7873=CARTESIAN_POINT('Origin',(-2.,1.25,-1.5));
#7874=CARTESIAN_POINT('',(-2.,1.25,-1.5));
#7875=CARTESIAN_POINT('Origin',(8.,0.,-1.5));
#9229=UNCERTAINTY_MEASURE_WITH_UNIT(LENGTH_MEASURE(0.001),#9286,
'DISTANCE_ACCURACY_VALUE',
'Maximum model space distance between geometric entities at asserted c
onnectivities');
#9255=UNCERTAINTY_MEASURE_WITH_UNIT(LENGTH_MEASURE(0.001),#9286,
'DISTANCE_ACCURACY_VALUE',
'Maximum model space distance between geometric entities at asserted c
onnectivities');
#9259=(
GEOMETRIC_REPRESENTATION_CONTEXT(3)
GLOBAL_UNCERTAINTY_ASSIGNED_CONTEXT((#9229))
GLOBAL_UNIT_ASSIGNED_CONTEXT((#9286,#9288,#9289))
REPRESENTATION_CONTEXT('','3D')
);
#9285=(
GEOMETRIC_REPRESENTATION_CONTEXT(3)
GLOBAL_UNCERTAINTY_ASSIGNED_CONTEXT((#9255))
GLOBAL_UNIT_ASSIGNED_CONTEXT((#9286,#9288,#9289))
REPRESENTATION_CONTEXT('','3D')
);
#9286=(
LENGTH_UNIT()
NAMED_UNIT(*)
SI_UNIT(.CENTI.,.METRE.)
);
#9288=(
NAMED_UNIT(*)
PLANE_ANGLE_UNIT()
SI_UNIT($,.RADIAN.)
);
#9289=(
NAMED_UNIT(*)
SI_UNIT($,.STERADIAN.)
SOLID_ANGLE_UNIT()
);
#9293=SHAPE_DEFINITION_REPRESENTATION(#9322,#9397);
#9322=PRODUCT_DEFINITION_SHAPE('',$,#9427);
#9397=SHAPE_REPRESENTATION('',(#5511),#9259);
#9423=PRODUCT_DEFINITION_CONTEXT('part definition',#9512,'design');
#9427=PRODUCT_DEFINITION('Bolt-clearance mounting stand',
'Bolt-clearance mounting stand',#9456,#9423);
#9456=PRODUCT_DEFINITION_FORMATION('',$,#9517);
#9512=APPLICATION_CONTEXT(
'Core Data for Automotive Mechanical Design Process');
#9513=PRODUCT_CONTEXT('part definition',#9512,'mechanical');
#9517=PRODUCT('Bolt-clearance mounting stand',
'Bolt-clearance mounting stand','Bolt-clearance mounting stand',(#9513));
#9613=COLOUR_RGB('Black',0.12,0.14,0.17);
#9614=FILL_AREA_STYLE_COLOUR('',#9613);
#9615=FILL_AREA_STYLE('',(#9614));
#9616=SURFACE_STYLE_FILL_AREA(#9615);
#9617=SURFACE_SIDE_STYLE('',(#9616));
#9618=SURFACE_STYLE_USAGE(.BOTH.,#9617);
#9619=PRESENTATION_STYLE_ASSIGNMENT((#9618));
ENDSEC;
END-ISO-10303-21;
